ISO-10303-21;
HEADER;
/* Generated by software containing ST-Developer
 * from STEP Tools, Inc. (www.steptools.com) 
 */

FILE_DESCRIPTION(
/* description */ ('STEP AP203'),
/* implementation_level */ '2;1');

FILE_NAME(
/* name */ 'P10_Lower_Feed_Screw.step',
/* time_stamp */ '2026-11-15T15:04:01-08:00',
/* author */ (''),
/* organization */ (''),
/* preprocessor_version */ 'ST-DEVELOPER v20.2',
/* originating_system */ 'Autodesk Translation Framework v15.17.0.0',
/* authorisation */ '');

FILE_SCHEMA (('AUTOMOTIVE_DESIGN { 1 0 10303 214 3 1 1 }'));
ENDSEC;

DATA;
#10=MECHANICAL_DESIGN_GEOMETRIC_PRESENTATION_REPRESENTATION('',(#289),#16598);
#211=SHAPE_REPRESENTATION_RELATIONSHIP('SRR','None',#16705,#235);
#235=ADVANCED_BREP_SHAPE_REPRESENTATION('',(#259),#16581);
#259=MANIFOLD_SOLID_BREP('Body1',#9794);
#289=STYLED_ITEM('',(#16831),#259);
#342=FACE_BOUND('',#1695,.T.);
#343=FACE_BOUND('',#1697,.T.);
#344=FACE_BOUND('',#1699,.T.);
#345=FACE_BOUND('',#1701,.T.);
#595=PLANE('',#10350);
#596=PLANE('',#10351);
#597=PLANE('',#10352);
#598=PLANE('',#10353);
#599=PLANE('',#10354);
#600=PLANE('',#10355);
#1101=FACE_OUTER_BOUND('',#1688,.T.);
#1102=FACE_OUTER_BOUND('',#1689,.T.);
#1103=FACE_OUTER_BOUND('',#1690,.T.);
#1104=FACE_OUTER_BOUND('',#1691,.T.);
#1105=FACE_OUTER_BOUND('',#1692,.T.);
#1106=FACE_OUTER_BOUND('',#1693,.T.);
#1107=FACE_OUTER_BOUND('',#1694,.T.);
#1108=FACE_OUTER_BOUND('',#1696,.T.);
#1109=FACE_OUTER_BOUND('',#1698,.T.);
#1110=FACE_OUTER_BOUND('',#1700,.T.);
#1111=FACE_OUTER_BOUND('',#1702,.T.);
#1688=EDGE_LOOP('',(#7557,#7558,#7559,#7560));
#1689=EDGE_LOOP('',(#7561,#7562,#7563,#7564));
#1690=EDGE_LOOP('',(#7565,#7566,#7567,#7568));
#1691=EDGE_LOOP('',(#7569,#7570,#7571,#7572));
#1692=EDGE_LOOP('',(#7573,#7574,#7575,#7576));
#1693=EDGE_LOOP('',(#7577));
#1694=EDGE_LOOP('',(#7578));
#1695=EDGE_LOOP('',(#7579));
#1696=EDGE_LOOP('',(#7580));
#1697=EDGE_LOOP('',(#7581));
#1698=EDGE_LOOP('',(#7582));
#1699=EDGE_LOOP('',(#7583));
#1700=EDGE_LOOP('',(#7584));
#1701=EDGE_LOOP('',(#7585));
#1702=EDGE_LOOP('',(#7586));
#2556=LINE('',#14683,#3604);
#2557=LINE('',#14689,#3605);
#2558=LINE('',#14695,#3606);
#2559=LINE('',#14701,#3607);
#2560=LINE('',#14707,#3608);
#3604=VECTOR('',#11870,5.55);
#3605=VECTOR('',#11877,6.);
#3606=VECTOR('',#11884,9.);
#3607=VECTOR('',#11891,6.);
#3608=VECTOR('',#11898,4.);
#4283=CIRCLE('',#10336,5.55);
#4284=CIRCLE('',#10337,5.55);
#4285=CIRCLE('',#10339,6.);
#4286=CIRCLE('',#10340,6.);
#4287=CIRCLE('',#10342,9.);
#4288=CIRCLE('',#10343,9.);
#4289=CIRCLE('',#10345,6.);
#4290=CIRCLE('',#10346,6.);
#4291=CIRCLE('',#10348,4.);
#4292=CIRCLE('',#10349,4.);
#4775=VERTEX_POINT('',#14680);
#4776=VERTEX_POINT('',#14682);
#4777=VERTEX_POINT('',#14686);
#4778=VERTEX_POINT('',#14688);
#4779=VERTEX_POINT('',#14692);
#4780=VERTEX_POINT('',#14694);
#4781=VERTEX_POINT('',#14698);
#4782=VERTEX_POINT('',#14700);
#4783=VERTEX_POINT('',#14704);
#4784=VERTEX_POINT('',#14706);
#5791=EDGE_CURVE('',#4775,#4775,#4283,.T.);
#5792=EDGE_CURVE('',#4775,#4776,#2556,.T.);
#5793=EDGE_CURVE('',#4776,#4776,#4284,.T.);
#5794=EDGE_CURVE('',#4777,#4777,#4285,.T.);
#5795=EDGE_CURVE('',#4777,#4778,#2557,.T.);
#5796=EDGE_CURVE('',#4778,#4778,#4286,.T.);
#5797=EDGE_CURVE('',#4779,#4779,#4287,.T.);
#5798=EDGE_CURVE('',#4779,#4780,#2558,.T.);
#5799=EDGE_CURVE('',#4780,#4780,#4288,.T.);
#5800=EDGE_CURVE('',#4781,#4781,#4289,.T.);
#5801=EDGE_CURVE('',#4781,#4782,#2559,.T.);
#5802=EDGE_CURVE('',#4782,#4782,#4290,.T.);
#5803=EDGE_CURVE('',#4783,#4783,#4291,.T.);
#5804=EDGE_CURVE('',#4783,#4784,#2560,.T.);
#5805=EDGE_CURVE('',#4784,#4784,#4292,.T.);
#7557=ORIENTED_EDGE('',*,*,#5791,.F.);
#7558=ORIENTED_EDGE('',*,*,#5792,.T.);
#7559=ORIENTED_EDGE('',*,*,#5793,.T.);
#7560=ORIENTED_EDGE('',*,*,#5792,.F.);
#7561=ORIENTED_EDGE('',*,*,#5794,.F.);
#7562=ORIENTED_EDGE('',*,*,#5795,.T.);
#7563=ORIENTED_EDGE('',*,*,#5796,.T.);
#7564=ORIENTED_EDGE('',*,*,#5795,.F.);
#7565=ORIENTED_EDGE('',*,*,#5797,.F.);
#7566=ORIENTED_EDGE('',*,*,#5798,.T.);
#7567=ORIENTED_EDGE('',*,*,#5799,.T.);
#7568=ORIENTED_EDGE('',*,*,#5798,.F.);
#7569=ORIENTED_EDGE('',*,*,#5800,.F.);
#7570=ORIENTED_EDGE('',*,*,#5801,.T.);
#7571=ORIENTED_EDGE('',*,*,#5802,.T.);
#7572=ORIENTED_EDGE('',*,*,#5801,.F.);
#7573=ORIENTED_EDGE('',*,*,#5803,.F.);
#7574=ORIENTED_EDGE('',*,*,#5804,.T.);
#7575=ORIENTED_EDGE('',*,*,#5805,.T.);
#7576=ORIENTED_EDGE('',*,*,#5804,.F.);
#7577=ORIENTED_EDGE('',*,*,#5803,.T.);
#7578=ORIENTED_EDGE('',*,*,#5800,.T.);
#7579=ORIENTED_EDGE('',*,*,#5805,.F.);
#7580=ORIENTED_EDGE('',*,*,#5797,.T.);
#7581=ORIENTED_EDGE('',*,*,#5802,.F.);
#7582=ORIENTED_EDGE('',*,*,#5799,.F.);
#7583=ORIENTED_EDGE('',*,*,#5794,.T.);
#7584=ORIENTED_EDGE('',*,*,#5796,.F.);
#7585=ORIENTED_EDGE('',*,*,#5791,.T.);
#7586=ORIENTED_EDGE('',*,*,#5793,.F.);
#9193=CYLINDRICAL_SURFACE('',#10335,5.55);
#9194=CYLINDRICAL_SURFACE('',#10338,6.);
#9195=CYLINDRICAL_SURFACE('',#10341,9.);
#9196=CYLINDRICAL_SURFACE('',#10344,6.);
#9197=CYLINDRICAL_SURFACE('',#10347,4.);
#9426=ADVANCED_FACE('',(#1101),#9193,.T.);
#9427=ADVANCED_FACE('',(#1102),#9194,.T.);
#9428=ADVANCED_FACE('',(#1103),#9195,.T.);
#9429=ADVANCED_FACE('',(#1104),#9196,.T.);
#9430=ADVANCED_FACE('',(#1105),#9197,.T.);
#9431=ADVANCED_FACE('',(#1106),#595,.F.);
#9432=ADVANCED_FACE('',(#1107,#342),#596,.F.);
#9433=ADVANCED_FACE('',(#1108,#343),#597,.F.);
#9434=ADVANCED_FACE('',(#1109,#344),#598,.F.);
#9435=ADVANCED_FACE('',(#1110,#345),#599,.F.);
#9436=ADVANCED_FACE('',(#1111),#600,.F.);
#9794=CLOSED_SHELL('',(#9426,#9427,#9428,#9429,#9430,#9431,#9432,#9433,
#9434,#9435,#9436));
#10334=AXIS2_PLACEMENT_3D('',#14678,#11864,#11865);
#10335=AXIS2_PLACEMENT_3D('',#14679,#11866,#11867);
#10336=AXIS2_PLACEMENT_3D('',#14681,#11868,#11869);
#10337=AXIS2_PLACEMENT_3D('',#14684,#11871,#11872);
#10338=AXIS2_PLACEMENT_3D('',#14685,#11873,#11874);
#10339=AXIS2_PLACEMENT_3D('',#14687,#11875,#11876);
#10340=AXIS2_PLACEMENT_3D('',#14690,#11878,#11879);
#10341=AXIS2_PLACEMENT_3D('',#14691,#11880,#11881);
#10342=AXIS2_PLACEMENT_3D('',#14693,#11882,#11883);
#10343=AXIS2_PLACEMENT_3D('',#14696,#11885,#11886);
#10344=AXIS2_PLACEMENT_3D('',#14697,#11887,#11888);
#10345=AXIS2_PLACEMENT_3D('',#14699,#11889,#11890);
#10346=AXIS2_PLACEMENT_3D('',#14702,#11892,#11893);
#10347=AXIS2_PLACEMENT_3D('',#14703,#11894,#11895);
#10348=AXIS2_PLACEMENT_3D('',#14705,#11896,#11897);
#10349=AXIS2_PLACEMENT_3D('',#14708,#11899,#11900);
#10350=AXIS2_PLACEMENT_3D('',#14709,#11901,#11902);
#10351=AXIS2_PLACEMENT_3D('',#14710,#11903,#11904);
#10352=AXIS2_PLACEMENT_3D('',#14711,#11905,#11906);
#10353=AXIS2_PLACEMENT_3D('',#14712,#11907,#11908);
#10354=AXIS2_PLACEMENT_3D('',#14713,#11909,#11910);
#10355=AXIS2_PLACEMENT_3D('',#14714,#11911,#11912);
#11864=DIRECTION('axis',(0.,0.,1.));
#11865=DIRECTION('refdir',(1.,0.,0.));
#11866=DIRECTION('center_axis',(0.,0.,-1.));
#11867=DIRECTION('ref_axis',(-1.,0.,0.));
#11868=DIRECTION('center_axis',(0.,0.,-1.));
#11869=DIRECTION('ref_axis',(-1.,0.,0.));
#11870=DIRECTION('',(0.,0.,1.));
#11871=DIRECTION('center_axis',(0.,0.,-1.));
#11872=DIRECTION('ref_axis',(-1.,0.,0.));
#11873=DIRECTION('center_axis',(0.,0.,-1.));
#11874=DIRECTION('ref_axis',(-1.,0.,0.));
#11875=DIRECTION('center_axis',(0.,0.,-1.));
#11876=DIRECTION('ref_axis',(-1.,0.,0.));
#11877=DIRECTION('',(0.,0.,1.));
#11878=DIRECTION('center_axis',(0.,0.,-1.));
#11879=DIRECTION('ref_axis',(-1.,0.,0.));
#11880=DIRECTION('center_axis',(0.,0.,-1.));
#11881=DIRECTION('ref_axis',(-1.,0.,0.));
#11882=DIRECTION('center_axis',(0.,0.,-1.));
#11883=DIRECTION('ref_axis',(-1.,0.,0.));
#11884=DIRECTION('',(0.,0.,1.));
#11885=DIRECTION('center_axis',(0.,0.,-1.));
#11886=DIRECTION('ref_axis',(-1.,0.,0.));
#11887=DIRECTION('center_axis',(0.,0.,-1.));
#11888=DIRECTION('ref_axis',(-1.,0.,0.));
#11889=DIRECTION('center_axis',(0.,0.,-1.));
#11890=DIRECTION('ref_axis',(-1.,0.,0.));
#11891=DIRECTION('',(0.,0.,1.));
#11892=DIRECTION('center_axis',(0.,0.,-1.));
#11893=DIRECTION('ref_axis',(-1.,0.,0.));
#11894=DIRECTION('center_axis',(0.,0.,-1.));
#11895=DIRECTION('ref_axis',(-1.,0.,0.));
#11896=DIRECTION('center_axis',(0.,0.,-1.));
#11897=DIRECTION('ref_axis',(-1.,0.,0.));
#11898=DIRECTION('',(0.,0.,1.));
#11899=DIRECTION('center_axis',(0.,0.,-1.));
#11900=DIRECTION('ref_axis',(-1.,0.,0.));
#11901=DIRECTION('center_axis',(0.,0.,1.));
#11902=DIRECTION('ref_axis',(1.,0.,0.));
#11903=DIRECTION('center_axis',(0.,0.,1.));
#11904=DIRECTION('ref_axis',(1.,0.,0.));
#11905=DIRECTION('center_axis',(0.,0.,1.));
#11906=DIRECTION('ref_axis',(1.,0.,0.));
#11907=DIRECTION('center_axis',(0.,0.,-1.));
#11908=DIRECTION('ref_axis',(-1.,0.,0.));
#11909=DIRECTION('center_axis',(0.,0.,-1.));
#11910=DIRECTION('ref_axis',(-1.,0.,0.));
#11911=DIRECTION('center_axis',(0.,0.,-1.));
#11912=DIRECTION('ref_axis',(-1.,0.,0.));
#14678=CARTESIAN_POINT('',(0.,0.,0.));
#14679=CARTESIAN_POINT('Origin',(0.,0.,-5.));
#14680=CARTESIAN_POINT('',(5.55,-6.79678973526781E-16,46.));
#14681=CARTESIAN_POINT('Origin',(0.,0.,46.));
#14682=CARTESIAN_POINT('',(5.55,-6.79678973526781E-16,260.));
#14683=CARTESIAN_POINT('',(5.55,-6.79678973526781E-16,-5.));
#14684=CARTESIAN_POINT('Origin',(0.,0.,260.));
#14685=CARTESIAN_POINT('Origin',(0.,0.,-5.));
#14686=CARTESIAN_POINT('',(6.,-7.34788079488412E-16,40.));
#14687=CARTESIAN_POINT('Origin',(0.,0.,40.));
#14688=CARTESIAN_POINT('',(6.,-7.34788079488412E-16,46.));
#14689=CARTESIAN_POINT('',(6.,-7.34788079488412E-16,-5.));
#14690=CARTESIAN_POINT('Origin',(0.,0.,46.));
#14691=CARTESIAN_POINT('Origin',(0.,0.,-5.));
#14692=CARTESIAN_POINT('',(9.,-1.10218211923262E-15,36.));
#14693=CARTESIAN_POINT('Origin',(0.,0.,36.));
#14694=CARTESIAN_POINT('',(9.,-1.10218211923262E-15,40.));
#14695=CARTESIAN_POINT('',(9.,-1.10218211923262E-15,-5.));
#14696=CARTESIAN_POINT('Origin',(0.,0.,40.));
#14697=CARTESIAN_POINT('Origin',(0.,0.,-5.));
#14698=CARTESIAN_POINT('',(6.,-7.34788079488412E-16,14.));
#14699=CARTESIAN_POINT('Origin',(0.,0.,14.));
#14700=CARTESIAN_POINT('',(6.,-7.34788079488412E-16,36.));
#14701=CARTESIAN_POINT('',(6.,-7.34788079488412E-16,-5.));
#14702=CARTESIAN_POINT('Origin',(0.,0.,36.));
#14703=CARTESIAN_POINT('Origin',(0.,0.,-5.));
#14704=CARTESIAN_POINT('',(4.,-4.89858719658941E-16,0.));
#14705=CARTESIAN_POINT('Origin',(0.,0.,0.));
#14706=CARTESIAN_POINT('',(4.,-4.89858719658941E-16,14.));
#14707=CARTESIAN_POINT('',(4.,-4.89858719658941E-16,-5.));
#14708=CARTESIAN_POINT('Origin',(0.,0.,14.));
#14709=CARTESIAN_POINT('Origin',(0.,0.,0.));
#14710=CARTESIAN_POINT('Origin',(4.,0.,14.));
#14711=CARTESIAN_POINT('Origin',(6.,0.,36.));
#14712=CARTESIAN_POINT('Origin',(9.,0.,40.));
#14713=CARTESIAN_POINT('Origin',(6.,0.,46.));
#14714=CARTESIAN_POINT('Origin',(5.55,0.,260.));
#16555=UNCERTAINTY_MEASURE_WITH_UNIT(LENGTH_MEASURE(0.01),#16599,
'DISTANCE_ACCURACY_VALUE',
'Maximum model space distance between geometric entities at asserted c
onnectivities');
#16572=UNCERTAINTY_MEASURE_WITH_UNIT(LENGTH_MEASURE(0.01),#16599,
'DISTANCE_ACCURACY_VALUE',
'Maximum model space distance between geometric entities at asserted c
onnectivities');
#16581=(
GEOMETRIC_REPRESENTATION_CONTEXT(3)
GLOBAL_UNCERTAINTY_ASSIGNED_CONTEXT((#16555))
GLOBAL_UNIT_ASSIGNED_CONTEXT((#16599,#16601,#16602))
REPRESENTATION_CONTEXT('','3D')
);
#16598=(
GEOMETRIC_REPRESENTATION_CONTEXT(3)
GLOBAL_UNCERTAINTY_ASSIGNED_CONTEXT((#16572))
GLOBAL_UNIT_ASSIGNED_CONTEXT((#16599,#16601,#16602))
REPRESENTATION_CONTEXT('','3D')
);
#16599=(
LENGTH_UNIT()
NAMED_UNIT(*)
SI_UNIT(.MILLI.,.METRE.)
);
#16601=(
NAMED_UNIT(*)
PLANE_ANGLE_UNIT()
SI_UNIT($,.RADIAN.)
);
#16602=(
NAMED_UNIT(*)
SI_UNIT($,.STERADIAN.)
SOLID_ANGLE_UNIT()
);
#16611=SHAPE_DEFINITION_REPRESENTATION(#16636,#16705);
#16636=PRODUCT_DEFINITION_SHAPE('',$,#16731);
#16705=SHAPE_REPRESENTATION('',(#10334),#16581);
#16722=PRODUCT_DEFINITION_CONTEXT('part definition',#16799,'design');
#16731=PRODUCT_DEFINITION('P10_Lower_Feed_Screw','P10_Lower_Feed_Screw',
#16756,#16722);
#16756=PRODUCT_DEFINITION_FORMATION('',$,#16809);
#16799=APPLICATION_CONTEXT(
'Core Data for Automotive Mechanical Design Process');
#16800=PRODUCT_CONTEXT('part definition',#16799,'mechanical');
#16809=PRODUCT('P10_Lower_Feed_Screw','P10_Lower_Feed_Screw',$,(#16800));
#16831=PRESENTATION_STYLE_ASSIGNMENT((#16840));
#16840=SURFACE_STYLE_USAGE(.BOTH.,#16849);
#16849=SURFACE_SIDE_STYLE('',(#16858));
#16858=SURFACE_STYLE_FILL_AREA(#16867);
#16867=FILL_AREA_STYLE('Black',(#16876));
#16876=FILL_AREA_STYLE_COLOUR('Black',#16885);
#16885=COLOUR_RGB('Black',0.0784313725490196,0.0784313725490196,0.0784313725490196);
ENDSEC;
END-ISO-10303-21;
